ISO-10303-21;
HEADER;
FILE_DESCRIPTION (('STEP AP203'),
    '1' );
FILE_NAME ('Aloris-BXA-Ball.step',
    '2026-10-07T20:09:13',
    ( '' ),
    ( '' ),
    'SwSTEP 2.0',
    'SolidWorks 2024',
    '' );
FILE_SCHEMA (( 'AUTOMOTIVE_DESIGN' ));
ENDSEC;

DATA;
#209=EDGE_CURVE ( 'NONE', #14671, #23965, #20865, .T. ) ;
#498=DIRECTION ( 'NONE',  ( -0.000000000000000000, -0.000000000000000000, -1.000000000000000000 ) ) ;
#707=CIRCLE ( 'NONE', #14345, 0.3150000000000000022 ) ;
#936=UNCERTAINTY_MEASURE_WITH_UNIT (LENGTH_MEASURE( 1.000000000000000082E-05 ), #21959, 'distance_accuracy_value', 'NONE');
#1000=FACE_OUTER_BOUND ( 'NONE', #18833, .T. ) ;
#1040=AXIS2_PLACEMENT_3D ( 'NONE', #16463, #12823, #22182 ) ;
#1049=CARTESIAN_POINT ( 'NONE',  ( 0.000000000000000000, 0.1199999999999999678, 0.000000000000000000 ) ) ;
#1058=VERTEX_POINT ( 'NONE', #17591 ) ;
#1119=ORIENTED_EDGE ( 'NONE', *, *, #3813, .T. ) ;
#1248=ORIENTED_EDGE ( 'NONE', *, *, #19558, .F. ) ;
#1273=EDGE_LOOP ( 'NONE', ( #4711, #3490 ) ) ;
#1343=CARTESIAN_POINT ( 'NONE',  ( 0.000000000000000000, 0.06786299768266475241, 0.000000000000000000 ) ) ;
#1593=DIRECTION ( 'NONE',  ( 0.000000000000000000, 1.000000000000000000, 0.000000000000000000 ) ) ;
#1640=ORIENTED_EDGE ( 'NONE', *, *, #14535, .F. ) ;
#1722=CARTESIAN_POINT ( 'NONE',  ( 0.3149999999999997802, 0.06786299768266475241, -3.857637417314159607E-17 ) ) ;
#1789=DIRECTION ( 'NONE',  ( -0.000000000000000000, -1.000000000000000000, -0.000000000000000000 ) ) ;
#1817=DIRECTION ( 'NONE',  ( 0.000000000000000000, -0.5150380749100549327, -0.8571673007021117785 ) ) ;
#1827=ADVANCED_FACE ( 'NONE', ( #9900 ), #22693, .T. ) ;
#1873=AXIS2_PLACEMENT_3D ( 'NONE', #18586, #7606, #18345 ) ;
#1901=EDGE_LOOP ( 'NONE', ( #1640, #11283, #22607, #1928 ) ) ;
#1928=ORIENTED_EDGE ( 'NONE', *, *, #3498, .F. ) ;
#2019=CARTESIAN_POINT ( 'NONE',  ( 0.000000000000000000, 0.1199999999999999956, -0.3150000000000000022 ) ) ;
#2054=DIRECTION ( 'NONE',  ( 0.000000000000000000, 0.000000000000000000, -1.000000000000000000 ) ) ;
#2065=DIRECTION ( 'NONE',  ( -1.224646799147353207E-16, 0.000000000000000000, -1.000000000000000000 ) ) ;
#2163=EDGE_CURVE ( 'NONE', #14885, #20299, #4639, .T. ) ;
#2178=EDGE_CURVE ( 'NONE', #23965, #1058, #6891, .T. ) ;
#2280=EDGE_CURVE ( 'NONE', #20305, #19663, #10409, .T. ) ;
#2530=LINE ( 'NONE', #13753, #2649 ) ;
#2577=CLOSED_SHELL ( 'NONE', ( #12468, #17079, #9619, #12370, #1827, #20856, #11804, #20389, #18255 ) ) ;
#2649=VECTOR ( 'NONE', #21178, 39.37007874015748143 ) ;
#2828=ORIENTED_EDGE ( 'NONE', *, *, #19144, .F. ) ;
#3138=AXIS2_PLACEMENT_3D ( 'NONE', #19026, #17311, #8036 ) ;
#3143=CARTESIAN_POINT ( 'NONE',  ( 2.583392422801336671E-17, 0.1199999999999999678, 0.2109499999999995268 ) ) ;
#3174=DIRECTION ( 'NONE',  ( 0.000000000000000000, 0.000000000000000000, 1.000000000000000000 ) ) ;
#3225=ORIENTED_EDGE ( 'NONE', *, *, #2178, .T. ) ;
#3447=DIRECTION ( 'NONE',  ( -0.000000000000000000, -1.000000000000000000, -0.000000000000000000 ) ) ;
#3475=CIRCLE ( 'NONE', #5426, 0.2109499999999995268 ) ;
#3490=ORIENTED_EDGE ( 'NONE', *, *, #7206, .F. ) ;
#3498=EDGE_CURVE ( 'NONE', #20299, #20305, #6057, .T. ) ;
#3572=FACE_OUTER_BOUND ( 'NONE', #18434, .T. ) ;
#3612=CONICAL_SURFACE ( 'NONE', #13761, 0.2109499999999998043, 1.029744258676653645 ) ;
#3693=AXIS2_PLACEMENT_3D ( 'NONE', #22291, #3884, #2054 ) ;
#3773=AXIS2_PLACEMENT_3D ( 'NONE', #22577, #498, #15386 ) ;
#3813=EDGE_CURVE ( 'NONE', #4009, #1058, #2530, .T. ) ;
#3866=CARTESIAN_POINT ( 'NONE',  ( 0.000000000000000000, 0.1199999999999999956, 0.000000000000000000 ) ) ;
#3884=DIRECTION ( 'NONE',  ( 0.000000000000000000, -1.000000000000000000, 0.000000000000000000 ) ) ;
#3893=CARTESIAN_POINT ( 'NONE',  ( -2.147421952792136087E-16, 0.9967515475838637506, 0.000000000000000000 ) ) ;
#4009=VERTEX_POINT ( 'NONE', #2019 ) ;
#4054=AXIS2_PLACEMENT_3D ( 'NONE', #17588, #21125, #15999 ) ;
#4139=PLANE ( 'NONE',  #3138 ) ;
#4181=ORIENTED_EDGE ( 'NONE', *, *, #3813, .F. ) ;
#4307=DIRECTION ( 'NONE',  ( -0.000000000000000000, 0.000000000000000000, 1.000000000000000000 ) ) ;
#4350=SHAPE_REPRESENTATION ( 'Aloris-BXA-Ball', ( #9127 ), #12664 ) ;
#4426=CARTESIAN_POINT ( 'NONE',  ( 0.000000000000000000, 0.06786299768266475241, 0.000000000000000000 ) ) ;
#4552=CARTESIAN_POINT ( 'NONE',  ( -4.684274006738626122E-17, 1.530000000000000027, 0.000000000000000000 ) ) ;
#4620=CARTESIAN_POINT ( 'NONE',  ( 0.000000000000000000, 0.1199999999999999956, 0.000000000000000000 ) ) ;
#4639=LINE ( 'NONE', #12105, #14292 ) ;
#4663=FACE_OUTER_BOUND ( 'NONE', #7853, .T. ) ;
#4711=ORIENTED_EDGE ( 'NONE', *, *, #2280, .F. ) ;
#4855=DIRECTION ( 'NONE',  ( 0.000000000000000000, 0.000000000000000000, 1.000000000000000000 ) ) ;
#4998=CARTESIAN_POINT ( 'NONE',  ( 3.857637417314162073E-17, 0.1199999999999999956, 0.3150000000000000022 ) ) ;
#5010=LINE ( 'NONE', #8428, #5037 ) ;
#5012=CARTESIAN_POINT ( 'NONE',  ( 2.583392422801339445E-17, 0.8699999999999998845, 0.2109499999999998043 ) ) ;
#5037=VECTOR ( 'NONE', #10633, 39.37007874015748143 ) ;
#5088=EDGE_CURVE ( 'NONE', #10393, #14932, #11234, .T. ) ;
#5119=EDGE_CURVE ( 'NONE', #1058, #14932, #707, .T. ) ;
#5334=DIRECTION ( 'NONE',  ( 0.000000000000000000, 0.000000000000000000, -1.000000000000000000 ) ) ;
#5426=AXIS2_PLACEMENT_3D ( 'NONE', #1049, #3447, #18209 ) ;
#5650=ORIENTED_EDGE ( 'NONE', *, *, #2163, .T. ) ;
#5678=EDGE_CURVE ( 'NONE', #14932, #14671, #19786, .T. ) ;
#5772=ORIENTED_EDGE ( 'NONE', *, *, #5088, .F. ) ;
#5777=ORIENTED_EDGE ( 'NONE', *, *, #10985, .T. ) ;
#5962=AXIS2_PLACEMENT_3D ( 'NONE', #3866, #1789, #22150 ) ;
#6057=LINE ( 'NONE', #20939, #8450 ) ;
#6321=DIRECTION ( 'NONE',  ( -0.000000000000000000, -1.000000000000000000, -0.000000000000000000 ) ) ;
#6386=CIRCLE ( 'NONE', #20017, 0.2109499999999998043 ) ;
#6632=EDGE_CURVE ( 'NONE', #19164, #14671, #18471, .T. ) ;
#6755=ORIENTED_EDGE ( 'NONE', *, *, #6632, .T. ) ;
#6891=CIRCLE ( 'NONE', #15834, 0.3150000000000000022 ) ;
#7136=ORIENTED_EDGE ( 'NONE', *, *, #19558, .T. ) ;
#7158=ORIENTED_EDGE ( 'NONE', *, *, #14535, .T. ) ;
#7182=ORIENTED_EDGE ( 'NONE', *, *, #2163, .F. ) ;
#7206=EDGE_CURVE ( 'NONE', #19663, #20305, #3475, .T. ) ;
#7214=( NAMED_UNIT ( * ) PLANE_ANGLE_UNIT ( ) SI_UNIT ( $, .RADIAN. ) );
#7338=CARTESIAN_POINT ( 'NONE',  ( 0.000000000000000000, 0.1199999999999999956, 0.000000000000000000 ) ) ;
#7606=DIRECTION ( 'NONE',  ( 0.000000000000000000, 1.000000000000000000, 0.000000000000000000 ) ) ;
#7813=DIRECTION ( 'NONE',  ( 0.000000000000000000, 0.000000000000000000, 1.000000000000000000 ) ) ;
#7853=EDGE_LOOP ( 'NONE', ( #5772, #5777, #3225, #18970 ) ) ;
#8036=DIRECTION ( 'NONE',  ( 0.000000000000000000, -0.000000000000000000, 1.000000000000000000 ) ) ;
#8067=DIRECTION ( 'NONE',  ( -0.000000000000000000, -1.000000000000000000, -0.000000000000000000 ) ) ;
#8145=CARTESIAN_POINT ( 'NONE',  ( 0.000000000000000000, 0.8699999999999998845, 0.000000000000000000 ) ) ;
#8397=EDGE_CURVE ( 'NONE', #20593, #19663, #5010, .T. ) ;
#8428=CARTESIAN_POINT ( 'NONE',  ( 2.583392422801337288E-17, 0.1199999999999999956, 0.2109499999999996656 ) ) ;
#8450=VECTOR ( 'NONE', #11684, 39.37007874015748143 ) ;
#8799=SPHERICAL_SURFACE ( 'NONE', #19501, 0.7650000000000000133 ) ;
#8861=ORIENTED_EDGE ( 'NONE', *, *, #6632, .F. ) ;
#8951=PRODUCT_DEFINITION_SHAPE ( 'NONE', 'NONE',  #19252 ) ;
#8982=ORIENTED_EDGE ( 'NONE', *, *, #5678, .F. ) ;
#8990=AXIS2_PLACEMENT_3D ( 'NONE', #7338, #20266, #22087 ) ;
#8998=DIRECTION ( 'NONE',  ( -0.000000000000000000, -1.000000000000000000, -0.000000000000000000 ) ) ;
#9073=DIRECTION ( 'NONE',  ( 1.049727191138618079E-16, -0.5150380749100549327, 0.8571673007021117785 ) ) ;
#9127=AXIS2_PLACEMENT_3D ( 'NONE', #15878, #23181, #23294 ) ;
#9159=LENGTH_MEASURE_WITH_UNIT ( LENGTH_MEASURE( 0.02539999999999999897 ), #21843 );
#9197=SHAPE_DEFINITION_REPRESENTATION ( #8951, #4350 ) ;
#9223=FACE_OUTER_BOUND ( 'NONE', #16796, .T. ) ;
#9232=CYLINDRICAL_SURFACE ( 'NONE', #5962, 0.2109499999999996656 ) ;
#9447=CARTESIAN_POINT ( 'NONE',  ( 3.857637417314162073E-17, 0.1199999999999999956, 0.3150000000000000022 ) ) ;
#9495=CYLINDRICAL_SURFACE ( 'NONE', #3693, 0.3150000000000000022 ) ;
#9619=ADVANCED_FACE ( 'NONE', ( #9223 ), #16662, .F. ) ;
#9646=CARTESIAN_POINT ( 'NONE',  ( 0.000000000000000000, 0.06786299768266475241, 0.000000000000000000 ) ) ;
#9717=EDGE_LOOP ( 'NONE', ( #16273, #1248, #17843, #23840 ) ) ;
#9900=FACE_OUTER_BOUND ( 'NONE', #23941, .T. ) ;
#10067=ORIENTED_EDGE ( 'NONE', *, *, #5678, .T. ) ;
#10393=VERTEX_POINT ( 'NONE', #4552 ) ;
#10409=CIRCLE ( 'NONE', #1040, 0.2109499999999995268 ) ;
#10538=AXIS2_PLACEMENT_3D ( 'NONE', #21663, #18009, #23595 ) ;
#10605=FACE_OUTER_BOUND ( 'NONE', #21009, .T. ) ;
#10633=DIRECTION ( 'NONE',  ( -0.000000000000000000, -1.000000000000000000, -0.000000000000000000 ) ) ;
#10799=LINE ( 'NONE', #18227, #12270 ) ;
#10985=EDGE_CURVE ( 'NONE', #10393, #23965, #13285, .T. ) ;
#11099=ORIENTED_EDGE ( 'NONE', *, *, #21699, .F. ) ;
#11234=CIRCLE ( 'NONE', #13197, 0.7650000000000000133 ) ;
#11283=ORIENTED_EDGE ( 'NONE', *, *, #8397, .T. ) ;
#11381=DIRECTION ( 'NONE',  ( 0.000000000000000000, 0.000000000000000000, -1.000000000000000000 ) ) ;
#11505=CARTESIAN_POINT ( 'NONE',  ( 0.000000000000000000, 0.8699999999999998845, 0.000000000000000000 ) ) ;
#11684=DIRECTION ( 'NONE',  ( -0.000000000000000000, -1.000000000000000000, -0.000000000000000000 ) ) ;
#11763=DIRECTION ( 'NONE',  ( 1.000000000000000000, 0.000000000000000000, 0.000000000000000000 ) ) ;
#11804=ADVANCED_FACE ( 'NONE', ( #13427, #3572 ), #4139, .F. ) ;
#12105=CARTESIAN_POINT ( 'NONE',  ( 0.000000000000000000, 0.8699999999999998845, -0.2109499999999998043 ) ) ;
#12237=ORIENTED_EDGE ( 'NONE', *, *, #19144, .T. ) ;
#12270=VECTOR ( 'NONE', #9073, 39.37007874015748143 ) ;
#12295=ORIENTED_EDGE ( 'NONE', *, *, #209, .T. ) ;
#12370=ADVANCED_FACE ( 'NONE', ( #4663 ), #8799, .T. ) ;
#12468=ADVANCED_FACE ( 'NONE', ( #13090 ), #16846, .F. ) ;
#12515=MECHANICAL_CONTEXT ( 'NONE', #13114, 'mechanical' ) ;
#12628=CIRCLE ( 'NONE', #13013, 0.3150000000000000022 ) ;
#12664=( GEOMETRIC_REPRESENTATION_CONTEXT ( 3 ) GLOBAL_UNCERTAINTY_ASSIGNED_CONTEXT ( ( #936 ) ) GLOBAL_UNIT_ASSIGNED_CONTEXT ( ( #21959, #7214, #23656 ) ) REPRESENTATION_CONTEXT ( 'NONE', 'WORKASPACE' ) );
#12823=DIRECTION ( 'NONE',  ( -0.000000000000000000, -1.000000000000000000, -0.000000000000000000 ) ) ;
#12881=AXIS2_PLACEMENT_3D ( 'NONE', #16805, #8998, #5334 ) ;
#13013=AXIS2_PLACEMENT_3D ( 'NONE', #4620, #23138, #4855 ) ;
#13028=AXIS2_PLACEMENT_3D ( 'NONE', #21586, #1593, #3174 ) ;
#13090=FACE_OUTER_BOUND ( 'NONE', #1901, .T. ) ;
#13114=APPLICATION_CONTEXT ( 'configuration controlled 3d designs of mechanical parts and assemblies' ) ;
#13197=AXIS2_PLACEMENT_3D ( 'NONE', #17125, #4307, #11763 ) ;
#13285=CIRCLE ( 'NONE', #14844, 0.7650000000000000133 ) ;
#13303=CARTESIAN_POINT ( 'NONE',  ( 0.000000000000000000, 0.7650000000000000133, 0.000000000000000000 ) ) ;
#13376=ORIENTED_EDGE ( 'NONE', *, *, #5088, .T. ) ;
#13427=FACE_BOUND ( 'NONE', #1273, .T. ) ;
#13753=CARTESIAN_POINT ( 'NONE',  ( 0.000000000000000000, 0.1199999999999999956, -0.3150000000000000022 ) ) ;
#13761=AXIS2_PLACEMENT_3D ( 'NONE', #11505, #8067, #11381 ) ;
#13828=DIRECTION ( 'NONE',  ( 0.000000000000000000, 0.000000000000000000, 1.000000000000000000 ) ) ;
#14292=VECTOR ( 'NONE', #1817, 39.37007874015748143 ) ;
#14345=AXIS2_PLACEMENT_3D ( 'NONE', #4426, #17245, #13828 ) ;
#14409=PRODUCT ( 'Aloris-BXA-Ball', 'Aloris-BXA-Ball', '', ( #12515 ) ) ;
#14444=ORIENTED_EDGE ( 'NONE', *, *, #2178, .F. ) ;
#14535=EDGE_CURVE ( 'NONE', #20593, #20299, #23349, .T. ) ;
#14671=VERTEX_POINT ( 'NONE', #23106 ) ;
#14844=AXIS2_PLACEMENT_3D ( 'NONE', #13303, #2065, #20838 ) ;
#14885=VERTEX_POINT ( 'NONE', #3893 ) ;
#14898=DIRECTION ( 'NONE',  ( 0.000000000000000000, 1.000000000000000000, 0.000000000000000000 ) ) ;
#14932=VERTEX_POINT ( 'NONE', #20241 ) ;
#14968=FACE_OUTER_BOUND ( 'NONE', #9717, .T. ) ;
#15164=CARTESIAN_POINT ( 'NONE',  ( 0.000000000000000000, 0.8699999999999998845, -0.2109499999999998043 ) ) ;
#15386=DIRECTION ( 'NONE',  ( -1.000000000000000000, 0.000000000000000000, 0.000000000000000000 ) ) ;
#15428=AXIS2_PLACEMENT_3D ( 'NONE', #9646, #14898, #7813 ) ;
#15721=CIRCLE ( 'NONE', #13028, 0.3150000000000000022 ) ;
#15834=AXIS2_PLACEMENT_3D ( 'NONE', #1343, #18408, #22063 ) ;
#15878=CARTESIAN_POINT ( 'NONE',  ( 0.000000000000000000, 0.000000000000000000, 0.000000000000000000 ) ) ;
#15999=DIRECTION ( 'NONE',  ( 0.000000000000000000, 0.000000000000000000, -1.000000000000000000 ) ) ;
#16169=EDGE_LOOP ( 'NONE', ( #7182, #21375, #7158 ) ) ;
#16250=DIRECTION ( 'NONE',  ( -0.000000000000000000, -0.000000000000000000, -1.000000000000000000 ) ) ;
#16273=ORIENTED_EDGE ( 'NONE', *, *, #8397, .F. ) ;
#16463=CARTESIAN_POINT ( 'NONE',  ( 0.000000000000000000, 0.1199999999999999678, 0.000000000000000000 ) ) ;
#16662=CYLINDRICAL_SURFACE ( 'NONE', #10538, 0.3150000000000000022 ) ;
#16796=EDGE_LOOP ( 'NONE', ( #22842, #6755, #8982, #20065, #4181 ) ) ;
#16805=CARTESIAN_POINT ( 'NONE',  ( 0.000000000000000000, 0.8699999999999998845, 0.000000000000000000 ) ) ;
#16846=CYLINDRICAL_SURFACE ( 'NONE', #8990, 0.2109499999999996656 ) ;
#17079=ADVANCED_FACE ( 'NONE', ( #19170 ), #3612, .F. ) ;
#17125=CARTESIAN_POINT ( 'NONE',  ( 0.000000000000000000, 0.7650000000000000133, 0.000000000000000000 ) ) ;
#17234=CARTESIAN_POINT ( 'NONE',  ( 0.000000000000000000, 0.1199999999999999678, -0.2109499999999995268 ) ) ;
#17245=DIRECTION ( 'NONE',  ( 0.000000000000000000, 1.000000000000000000, 0.000000000000000000 ) ) ;
#17311=DIRECTION ( 'NONE',  ( 0.000000000000000000, 1.000000000000000000, 0.000000000000000000 ) ) ;
#17529=MANIFOLD_SOLID_BREP ( '1/2-13 Tapped Hole1', #2577 ) ;
#17588=CARTESIAN_POINT ( 'NONE',  ( 0.000000000000000000, 0.8699999999999998845, 0.000000000000000000 ) ) ;
#17591=CARTESIAN_POINT ( 'NONE',  ( 0.000000000000000000, 0.06786299768266475241, -0.3150000000000000022 ) ) ;
#17594=CARTESIAN_POINT ( 'NONE',  ( 0.000000000000000000, 0.7650000000000000133, 0.000000000000000000 ) ) ;
#17744=PRODUCT_DEFINITION_FORMATION_WITH_SPECIFIED_SOURCE ( 'ANY', '', #14409, .NOT_KNOWN. ) ;
#17843=ORIENTED_EDGE ( 'NONE', *, *, #3498, .T. ) ;
#17863=EDGE_CURVE ( 'NONE', #4009, #19164, #12628, .T. ) ;
#18009=DIRECTION ( 'NONE',  ( 0.000000000000000000, -1.000000000000000000, 0.000000000000000000 ) ) ;
#18190=SHAPE_REPRESENTATION_RELATIONSHIP ( 'NONE' , 'NONE' ,  #4350, #22505 ) ;
#18209=DIRECTION ( 'NONE',  ( 0.000000000000000000, 0.000000000000000000, -1.000000000000000000 ) ) ;
#18227=CARTESIAN_POINT ( 'NONE',  ( 2.583392422801339445E-17, 0.8699999999999998845, 0.2109499999999998043 ) ) ;
#18255=ADVANCED_FACE ( 'NONE', ( #14968 ), #9232, .F. ) ;
#18345=DIRECTION ( 'NONE',  ( 0.000000000000000000, 0.000000000000000000, 1.000000000000000000 ) ) ;
#18408=DIRECTION ( 'NONE',  ( 0.000000000000000000, 1.000000000000000000, 0.000000000000000000 ) ) ;
#18434=EDGE_LOOP ( 'NONE', ( #21126, #2828 ) ) ;
#18471=LINE ( 'NONE', #9447, #22537 ) ;
#18586=CARTESIAN_POINT ( 'NONE',  ( 0.000000000000000000, 0.06786299768266475241, 0.000000000000000000 ) ) ;
#18833=EDGE_LOOP ( 'NONE', ( #11099, #5650, #7136 ) ) ;
#18970=ORIENTED_EDGE ( 'NONE', *, *, #5119, .T. ) ;
#19026=CARTESIAN_POINT ( 'NONE',  ( 0.000000000000000000, 0.1199999999999999956, 0.000000000000000000 ) ) ;
#19144=EDGE_CURVE ( 'NONE', #19164, #4009, #15721, .T. ) ;
#19164=VERTEX_POINT ( 'NONE', #4998 ) ;
#19170=FACE_OUTER_BOUND ( 'NONE', #16169, .T. ) ;
#19234=DESIGN_CONTEXT ( 'detailed design', #23822, 'design' ) ;
#19252=PRODUCT_DEFINITION ( 'UNKNOWN', '', #17744, #19234 ) ;
#19487=DIRECTION ( 'NONE',  ( 0.000000000000000000, 0.000000000000000000, -1.000000000000000000 ) ) ;
#19501=AXIS2_PLACEMENT_3D ( 'NONE', #17594, #16250, #23660 ) ;
#19558=EDGE_CURVE ( 'NONE', #20299, #20593, #6386, .T. ) ;
#19663=VERTEX_POINT ( 'NONE', #3143 ) ;
#19786=CIRCLE ( 'NONE', #1873, 0.3150000000000000022 ) ;
#20017=AXIS2_PLACEMENT_3D ( 'NONE', #8145, #6321, #19487 ) ;
#20065=ORIENTED_EDGE ( 'NONE', *, *, #5119, .F. ) ;
#20241=CARTESIAN_POINT ( 'NONE',  ( -0.3149999999999997802, 0.06786299768266475241, 0.000000000000000000 ) ) ;
#20266=DIRECTION ( 'NONE',  ( -0.000000000000000000, -1.000000000000000000, -0.000000000000000000 ) ) ;
#20299=VERTEX_POINT ( 'NONE', #15164 ) ;
#20305=VERTEX_POINT ( 'NONE', #17234 ) ;
#20389=ADVANCED_FACE ( 'NONE', ( #1000 ), #21198, .F. ) ;
#20593=VERTEX_POINT ( 'NONE', #5012 ) ;
#20660=DIRECTION ( 'NONE',  ( 0.000000000000000000, -1.000000000000000000, 0.000000000000000000 ) ) ;
#20838=DIRECTION ( 'NONE',  ( -1.000000000000000000, 0.000000000000000000, 1.224646799147353207E-16 ) ) ;
#20856=ADVANCED_FACE ( 'NONE', ( #10605 ), #9495, .F. ) ;
#20865=CIRCLE ( 'NONE', #15428, 0.3150000000000000022 ) ;
#20939=CARTESIAN_POINT ( 'NONE',  ( 0.000000000000000000, 0.1199999999999999956, -0.2109499999999996656 ) ) ;
#21009=EDGE_LOOP ( 'NONE', ( #8861, #12237, #1119, #14444, #22167 ) ) ;
#21125=DIRECTION ( 'NONE',  ( -0.000000000000000000, -1.000000000000000000, -0.000000000000000000 ) ) ;
#21126=ORIENTED_EDGE ( 'NONE', *, *, #17863, .F. ) ;
#21178=DIRECTION ( 'NONE',  ( 0.000000000000000000, -1.000000000000000000, 0.000000000000000000 ) ) ;
#21198=CONICAL_SURFACE ( 'NONE', #4054, 0.2109499999999998043, 1.029744258676653645 ) ;
#21375=ORIENTED_EDGE ( 'NONE', *, *, #21699, .T. ) ;
#21586=CARTESIAN_POINT ( 'NONE',  ( 0.000000000000000000, 0.1199999999999999956, 0.000000000000000000 ) ) ;
#21663=CARTESIAN_POINT ( 'NONE',  ( 0.000000000000000000, 0.1199999999999999956, 0.000000000000000000 ) ) ;
#21699=EDGE_CURVE ( 'NONE', #14885, #20593, #10799, .T. ) ;
#21843=( LENGTH_UNIT ( ) NAMED_UNIT ( * ) SI_UNIT ( $, .METRE. ) );
#21959=( CONVERSION_BASED_UNIT ( 'INCH', #9159 ) LENGTH_UNIT ( ) NAMED_UNIT ( #23314 ) );
#22063=DIRECTION ( 'NONE',  ( 0.000000000000000000, 0.000000000000000000, 1.000000000000000000 ) ) ;
#22087=DIRECTION ( 'NONE',  ( 0.000000000000000000, 0.000000000000000000, -1.000000000000000000 ) ) ;
#22150=DIRECTION ( 'NONE',  ( 0.000000000000000000, 0.000000000000000000, -1.000000000000000000 ) ) ;
#22167=ORIENTED_EDGE ( 'NONE', *, *, #209, .F. ) ;
#22182=DIRECTION ( 'NONE',  ( 0.000000000000000000, 0.000000000000000000, -1.000000000000000000 ) ) ;
#22239=ORIENTED_EDGE ( 'NONE', *, *, #10985, .F. ) ;
#22291=CARTESIAN_POINT ( 'NONE',  ( 0.000000000000000000, 0.1199999999999999956, 0.000000000000000000 ) ) ;
#22505=ADVANCED_BREP_SHAPE_REPRESENTATION ( '', ( #17529, #9127 ), #12664 ) ;
#22537=VECTOR ( 'NONE', #20660, 39.37007874015748143 ) ;
#22577=CARTESIAN_POINT ( 'NONE',  ( 0.000000000000000000, 0.7650000000000000133, 0.000000000000000000 ) ) ;
#22607=ORIENTED_EDGE ( 'NONE', *, *, #7206, .T. ) ;
#22693=SPHERICAL_SURFACE ( 'NONE', #3773, 0.7650000000000000133 ) ;
#22842=ORIENTED_EDGE ( 'NONE', *, *, #17863, .T. ) ;
#23106=CARTESIAN_POINT ( 'NONE',  ( 3.857637417314162073E-17, 0.06786299768266475241, 0.3150000000000000022 ) ) ;
#23138=DIRECTION ( 'NONE',  ( 0.000000000000000000, 1.000000000000000000, 0.000000000000000000 ) ) ;
#23181=DIRECTION ( 'NONE',  ( 0.000000000000000000, 0.000000000000000000, 1.000000000000000000 ) ) ;
#23294=DIRECTION ( 'NONE',  ( 1.000000000000000000, 0.000000000000000000, 0.000000000000000000 ) ) ;
#23314=DIMENSIONAL_EXPONENTS ( 1.000000000000000000, 0.000000000000000000, 0.000000000000000000, 0.000000000000000000, 0.000000000000000000, 0.000000000000000000, 0.000000000000000000 ) ;
#23349=CIRCLE ( 'NONE', #12881, 0.2109499999999998043 ) ;
#23595=DIRECTION ( 'NONE',  ( 0.000000000000000000, 0.000000000000000000, -1.000000000000000000 ) ) ;
#23656=( NAMED_UNIT ( * ) SI_UNIT ( $, .STERADIAN. ) SOLID_ANGLE_UNIT ( ) );
#23660=DIRECTION ( 'NONE',  ( -1.000000000000000000, 0.000000000000000000, 0.000000000000000000 ) ) ;
#23822=APPLICATION_CONTEXT ( 'configuration controlled 3d designs of mechanical parts and assemblies' ) ;
#23840=ORIENTED_EDGE ( 'NONE', *, *, #2280, .T. ) ;
#23941=EDGE_LOOP ( 'NONE', ( #22239, #13376, #10067, #12295 ) ) ;
#23965=VERTEX_POINT ( 'NONE', #1722 ) ;
#24145=COLOUR_RGB('Light Blue', 0.31764706, 0.68627451, 0.89019608);
#24146=FILL_AREA_STYLE_COLOUR('',#24145);
#24147=FILL_AREA_STYLE('',(#24146));
#24148=SURFACE_STYLE_FILL_AREA(#24147);
#24149=SURFACE_SIDE_STYLE('',(#24148));
#24150=SURFACE_STYLE_USAGE(.BOTH.,#24149);
#24151=PRESENTATION_STYLE_ASSIGNMENT((#24150));
#24194=STYLED_ITEM('',(#24151),#17529);
#24195=MECHANICAL_DESIGN_GEOMETRIC_PRESENTATION_REPRESENTATION('',(#24194),#12664);
ENDSEC;
END-ISO-10303-21;
